ISO-10303-21;
HEADER;
/* Generated by software containing ST-Developer
 * from STEP Tools, Inc. (www.steptools.com) 
 */

FILE_DESCRIPTION(
/* description */ ('Cam-driven reciprocating slide'),
/* implementation_level */ '2;1');

FILE_NAME(
/* name */ 'Spring seat washer.step',
/* time_stamp */ '2026-10-28T03:25:20-07:00',
/* author */ (''),
/* organization */ (''),
/* preprocessor_version */ 'ST-DEVELOPER v20.2',
/* originating_system */ 'Autodesk Translation Framework v15.17.0.0',
/* authorisation */ '');

FILE_SCHEMA (('AUTOMOTIVE_DESIGN { 1 0 10303 214 3 1 1 }'));
ENDSEC;

DATA;
#10=MECHANICAL_DESIGN_GEOMETRIC_PRESENTATION_REPRESENTATION('',(#465),#13277);
#384=SHAPE_REPRESENTATION_RELATIONSHIP('SRR','None',#13481,#421);
#421=ADVANCED_BREP_SHAPE_REPRESENTATION('',(#506),#13276);
#465=STYLED_ITEM('',(#13727),#506);
#506=MANIFOLD_SOLID_BREP('Body1',#6444);
#679=FACE_BOUND('',#1830,.T.);
#680=FACE_BOUND('',#1832,.T.);
#899=PLANE('',#7661);
#900=PLANE('',#7662);
#1276=FACE_OUTER_BOUND('',#1827,.T.);
#1277=FACE_OUTER_BOUND('',#1828,.T.);
#1278=FACE_OUTER_BOUND('',#1829,.T.);
#1279=FACE_OUTER_BOUND('',#1831,.T.);
#1827=EDGE_LOOP('',(#5880,#5881,#5882,#5883));
#1828=EDGE_LOOP('',(#5884,#5885,#5886,#5887));
#1829=EDGE_LOOP('',(#5888));
#1830=EDGE_LOOP('',(#5889));
#1831=EDGE_LOOP('',(#5890));
#1832=EDGE_LOOP('',(#5891));
#2270=LINE('',#13174,#2709);
#2271=LINE('',#13180,#2710);
#2709=VECTOR('',#9714,0.605);
#2710=VECTOR('',#9721,1.25);
#3031=CIRCLE('',#7656,0.605);
#3032=CIRCLE('',#7657,0.605);
#3033=CIRCLE('',#7659,1.25);
#3034=CIRCLE('',#7660,1.25);
#3554=VERTEX_POINT('',#13171);
#3555=VERTEX_POINT('',#13173);
#3556=VERTEX_POINT('',#13177);
#3557=VERTEX_POINT('',#13179);
#4330=EDGE_CURVE('',#3554,#3554,#3031,.T.);
#4331=EDGE_CURVE('',#3554,#3555,#2270,.T.);
#4332=EDGE_CURVE('',#3555,#3555,#3032,.T.);
#4333=EDGE_CURVE('',#3556,#3556,#3033,.T.);
#4334=EDGE_CURVE('',#3556,#3557,#2271,.T.);
#4335=EDGE_CURVE('',#3557,#3557,#3034,.T.);
#5880=ORIENTED_EDGE('',*,*,#4330,.F.);
#5881=ORIENTED_EDGE('',*,*,#4331,.T.);
#5882=ORIENTED_EDGE('',*,*,#4332,.T.);
#5883=ORIENTED_EDGE('',*,*,#4331,.F.);
#5884=ORIENTED_EDGE('',*,*,#4333,.F.);
#5885=ORIENTED_EDGE('',*,*,#4334,.T.);
#5886=ORIENTED_EDGE('',*,*,#4335,.T.);
#5887=ORIENTED_EDGE('',*,*,#4334,.F.);
#5888=ORIENTED_EDGE('',*,*,#4333,.T.);
#5889=ORIENTED_EDGE('',*,*,#4330,.T.);
#5890=ORIENTED_EDGE('',*,*,#4335,.F.);
#5891=ORIENTED_EDGE('',*,*,#4332,.F.);
#6017=CYLINDRICAL_SURFACE('',#7655,0.605);
#6018=CYLINDRICAL_SURFACE('',#7658,1.25);
#6394=ADVANCED_FACE('',(#1276),#6017,.F.);
#6395=ADVANCED_FACE('',(#1277),#6018,.T.);
#6396=ADVANCED_FACE('',(#1278,#679),#899,.T.);
#6397=ADVANCED_FACE('',(#1279,#680),#900,.F.);
#6444=CLOSED_SHELL('',(#6394,#6395,#6396,#6397));
#7654=AXIS2_PLACEMENT_3D('',#13169,#9708,#9709);
#7655=AXIS2_PLACEMENT_3D('',#13170,#9710,#9711);
#7656=AXIS2_PLACEMENT_3D('',#13172,#9712,#9713);
#7657=AXIS2_PLACEMENT_3D('',#13175,#9715,#9716);
#7658=AXIS2_PLACEMENT_3D('',#13176,#9717,#9718);
#7659=AXIS2_PLACEMENT_3D('',#13178,#9719,#9720);
#7660=AXIS2_PLACEMENT_3D('',#13181,#9722,#9723);
#7661=AXIS2_PLACEMENT_3D('',#13182,#9724,#9725);
#7662=AXIS2_PLACEMENT_3D('',#13183,#9726,#9727);
#9708=DIRECTION('axis',(0.,0.,1.));
#9709=DIRECTION('refdir',(1.,0.,0.));
#9710=DIRECTION('center_axis',(0.,0.,1.));
#9711=DIRECTION('ref_axis',(1.,0.,0.));
#9712=DIRECTION('center_axis',(0.,0.,-1.));
#9713=DIRECTION('ref_axis',(1.,0.,0.));
#9714=DIRECTION('',(0.,0.,-1.));
#9715=DIRECTION('center_axis',(0.,0.,-1.));
#9716=DIRECTION('ref_axis',(1.,0.,0.));
#9717=DIRECTION('center_axis',(0.,0.,1.));
#9718=DIRECTION('ref_axis',(1.,0.,0.));
#9719=DIRECTION('center_axis',(0.,0.,1.));
#9720=DIRECTION('ref_axis',(1.,0.,0.));
#9721=DIRECTION('',(0.,0.,-1.));
#9722=DIRECTION('center_axis',(0.,0.,1.));
#9723=DIRECTION('ref_axis',(1.,0.,0.));
#9724=DIRECTION('center_axis',(0.,0.,1.));
#9725=DIRECTION('ref_axis',(1.,0.,0.));
#9726=DIRECTION('center_axis',(0.,0.,1.));
#9727=DIRECTION('ref_axis',(1.,0.,0.));
#13169=CARTESIAN_POINT('',(0.,0.,0.));
#13170=CARTESIAN_POINT('Origin',(0.,0.,7.6));
#13171=CARTESIAN_POINT('',(-0.605,-7.40911313484149E-17,7.8));
#13172=CARTESIAN_POINT('Origin',(0.,0.,7.8));
#13173=CARTESIAN_POINT('',(-0.605,-7.40911313484149E-17,7.6));
#13174=CARTESIAN_POINT('',(-0.605,-7.40911313484149E-17,7.6));
#13175=CARTESIAN_POINT('Origin',(0.,0.,7.6));
#13176=CARTESIAN_POINT('Origin',(0.,0.,7.6));
#13177=CARTESIAN_POINT('',(-1.25,-1.53080849893419E-16,7.8));
#13178=CARTESIAN_POINT('Origin',(0.,0.,7.8));
#13179=CARTESIAN_POINT('',(-1.25,-1.53080849893419E-16,7.6));
#13180=CARTESIAN_POINT('',(-1.25,-1.53080849893419E-16,7.6));
#13181=CARTESIAN_POINT('Origin',(0.,0.,7.6));
#13182=CARTESIAN_POINT('Origin',(0.,0.,7.8));
#13183=CARTESIAN_POINT('Origin',(0.,0.,7.6));
#13232=UNCERTAINTY_MEASURE_WITH_UNIT(LENGTH_MEASURE(0.001),#13278,
'DISTANCE_ACCURACY_VALUE',
'Maximum model space distance between geometric entities at asserted c
onnectivities');
#13233=UNCERTAINTY_MEASURE_WITH_UNIT(LENGTH_MEASURE(0.001),#13278,
'DISTANCE_ACCURACY_VALUE',
'Maximum model space distance between geometric entities at asserted c
onnectivities');
#13276=(
GEOMETRIC_REPRESENTATION_CONTEXT(3)
GLOBAL_UNCERTAINTY_ASSIGNED_CONTEXT((#13232))
GLOBAL_UNIT_ASSIGNED_CONTEXT((#13278,#13280,#13281))
REPRESENTATION_CONTEXT('','3D')
);
#13277=(
GEOMETRIC_REPRESENTATION_CONTEXT(3)
GLOBAL_UNCERTAINTY_ASSIGNED_CONTEXT((#13233))
GLOBAL_UNIT_ASSIGNED_CONTEXT((#13278,#13280,#13281))
REPRESENTATION_CONTEXT('','3D')
);
#13278=(
LENGTH_UNIT()
NAMED_UNIT(*)
SI_UNIT(.CENTI.,.METRE.)
);
#13280=(
NAMED_UNIT(*)
PLANE_ANGLE_UNIT()
SI_UNIT($,.RADIAN.)
);
#13281=(
NAMED_UNIT(*)
SI_UNIT($,.STERADIAN.)
SOLID_ANGLE_UNIT()
);
#13324=SHAPE_DEFINITION_REPRESENTATION(#13432,#13481);
#13432=PRODUCT_DEFINITION_SHAPE('',$,#13525);
#13481=SHAPE_REPRESENTATION('',(#7654),#13276);
#13482=PRODUCT_DEFINITION_CONTEXT('part definition',#13613,'design');
#13525=PRODUCT_DEFINITION('Spring seat washer','Spring seat washer',#13568,
#13482);
#13568=PRODUCT_DEFINITION_FORMATION('',$,#13657);
#13613=APPLICATION_CONTEXT(
'Core Data for Automotive Mechanical Design Process');
#13614=PRODUCT_CONTEXT('part definition',#13613,'mechanical');
#13657=PRODUCT('Spring seat washer','Spring seat washer',
'Spring seat washer',(#13614));
#13721=COLOUR_RGB('Black',0.12,0.14,0.17);
#13722=FILL_AREA_STYLE_COLOUR('',#13721);
#13723=FILL_AREA_STYLE('',(#13722));
#13724=SURFACE_STYLE_FILL_AREA(#13723);
#13725=SURFACE_SIDE_STYLE('',(#13724));
#13726=SURFACE_STYLE_USAGE(.BOTH.,#13725);
#13727=PRESENTATION_STYLE_ASSIGNMENT((#13726));
ENDSEC;
END-ISO-10303-21;
